ISO-10303-21;
HEADER;
/* Generated by software containing ST-Developer
 * from STEP Tools, Inc. (www.steptools.com) 
 */

FILE_DESCRIPTION(
/* description */ (''),
/* implementation_level */ '2;1');

FILE_NAME(
/* name */ 'Ball_02.step',
/* time_stamp */ '2026-10-06T12:47:13-07:00',
/* author */ (''),
/* organization */ (''),
/* preprocessor_version */ 'ST-DEVELOPER v20.2',
/* originating_system */ 'Autodesk Translation Framework v15.15.0.0',
/* authorisation */ '');

FILE_SCHEMA (('AUTOMOTIVE_DESIGN { 1 0 10303 214 3 1 1 }'));
ENDSEC;

DATA;
#10=MECHANICAL_DESIGN_GEOMETRIC_PRESENTATION_REPRESENTATION('',(#69),#42667);
#47=SPHERICAL_SURFACE('',#4234,10.);
#51=SHAPE_REPRESENTATION_RELATIONSHIP('SRR','None',#42704,#60);
#60=ADVANCED_BREP_SHAPE_REPRESENTATION('',(#78),#42660);
#69=STYLED_ITEM('',(#42756),#78);
#78=MANIFOLD_SOLID_BREP('Body1',#4034);
#560=CIRCLE('',#4233,9.1643052178268);
#685=FACE_OUTER_BOUND('',#892,.T.);
#686=FACE_OUTER_BOUND('',#893,.T.);
#892=EDGE_LOOP('',(#2742));
#893=EDGE_LOOP('',(#2743));
#1542=VERTEX_POINT('',#5948);
#2022=EDGE_CURVE('',#1542,#1542,#560,.T.);
#2742=ORIENTED_EDGE('',*,*,#2022,.F.);
#2743=ORIENTED_EDGE('',*,*,#2022,.T.);
#3797=PLANE('',#4232);
#3881=ADVANCED_FACE('',(#685),#3797,.T.);
#3882=ADVANCED_FACE('',(#686),#47,.T.);
#4034=CLOSED_SHELL('',(#3881,#3882));
#4231=AXIS2_PLACEMENT_3D('',#5946,#4704,#4705);
#4232=AXIS2_PLACEMENT_3D('',#5947,#4706,#4707);
#4233=AXIS2_PLACEMENT_3D('',#5949,#4708,#4709);
#4234=AXIS2_PLACEMENT_3D('',#5950,#4710,#4711);
#4704=DIRECTION('axis',(0.,0.,1.));
#4705=DIRECTION('refdir',(1.,0.,0.));
#4706=DIRECTION('center_axis',(0.,-1.,0.));
#4707=DIRECTION('ref_axis',(0.,0.,-1.));
#4708=DIRECTION('center_axis',(0.,1.,0.));
#4709=DIRECTION('ref_axis',(1.,0.,0.));
#4710=DIRECTION('center_axis',(1.22464679914735E-16,0.,1.));
#4711=DIRECTION('ref_axis',(1.,0.,-6.12323399573677E-17));
#5946=CARTESIAN_POINT('',(0.,0.,0.));
#5947=CARTESIAN_POINT('Origin',(0.,4.0019382647053,9.1643052178268));
#5948=CARTESIAN_POINT('',(0.,4.0019382647053,9.1643052178268));
#5949=CARTESIAN_POINT('Origin',(0.,4.0019382647053,0.));
#5950=CARTESIAN_POINT('Origin',(0.,0.,0.));
#42649=UNCERTAINTY_MEASURE_WITH_UNIT(LENGTH_MEASURE(0.01),#42668,
'DISTANCE_ACCURACY_VALUE',
'Maximum model space distance between geometric entities at asserted c
onnectivities');
#42656=UNCERTAINTY_MEASURE_WITH_UNIT(LENGTH_MEASURE(0.01),#42668,
'DISTANCE_ACCURACY_VALUE',
'Maximum model space distance between geometric entities at asserted c
onnectivities');
#42660=(
GEOMETRIC_REPRESENTATION_CONTEXT(3)
GLOBAL_UNCERTAINTY_ASSIGNED_CONTEXT((#42649))
GLOBAL_UNIT_ASSIGNED_CONTEXT((#42668,#42670,#42671))
REPRESENTATION_CONTEXT('','3D')
);
#42667=(
GEOMETRIC_REPRESENTATION_CONTEXT(3)
GLOBAL_UNCERTAINTY_ASSIGNED_CONTEXT((#42656))
GLOBAL_UNIT_ASSIGNED_CONTEXT((#42668,#42670,#42671))
REPRESENTATION_CONTEXT('','3D')
);
#42668=(
LENGTH_UNIT()
NAMED_UNIT(*)
SI_UNIT(.MILLI.,.METRE.)
);
#42670=(
NAMED_UNIT(*)
PLANE_ANGLE_UNIT()
SI_UNIT($,.RADIAN.)
);
#42671=(
NAMED_UNIT(*)
SI_UNIT($,.STERADIAN.)
SOLID_ANGLE_UNIT()
);
#42675=SHAPE_DEFINITION_REPRESENTATION(#42685,#42704);
#42685=PRODUCT_DEFINITION_SHAPE('',$,#42715);
#42704=SHAPE_REPRESENTATION('',(#4231),#42660);
#42711=PRODUCT_DEFINITION_CONTEXT('part definition',#42743,'design');
#42715=PRODUCT_DEFINITION('Ball_02','Ball_02',#42725,#42711);
#42725=PRODUCT_DEFINITION_FORMATION('',$,#42748);
#42743=APPLICATION_CONTEXT(
'Core Data for Automotive Mechanical Design Process');
#42744=PRODUCT_CONTEXT('part definition',#42743,'mechanical');
#42748=PRODUCT('Ball_02','Ball_02',$,(#42744));
#42756=PRESENTATION_STYLE_ASSIGNMENT((#42758));
#42758=SURFACE_STYLE_USAGE(.BOTH.,#42760);
#42760=SURFACE_SIDE_STYLE('',(#42762));
#42762=SURFACE_STYLE_FILL_AREA(#42764);
#42764=FILL_AREA_STYLE('Opaque(160,160,160)',(#42766));
#42766=FILL_AREA_STYLE_COLOUR('Opaque(160,160,160)',#42768);
#42768=COLOUR_RGB('Opaque(160,160,160)', 0.09019608, 0.27058824, 0.51372549);
ENDSEC;
END-ISO-10303-21;
